ISO-10303-21;
HEADER;
/* Generated by software containing ST-Developer
 * from STEP Tools, Inc. (www.steptools.com) 
 */

FILE_DESCRIPTION(
/* description */ ('Four-wheel beam trolley'),
/* implementation_level */ '2;1');

FILE_NAME(
/* name */ 'Flat Washer - M8.step',
/* time_stamp */ '2026-10-29T16:22:06-07:00',
/* author */ (''),
/* organization */ (''),
/* preprocessor_version */ 'ST-DEVELOPER v20.2',
/* originating_system */ 'Autodesk Translation Framework v15.17.0.0',
/* authorisation */ '');

FILE_SCHEMA (('AUTOMOTIVE_DESIGN { 1 0 10303 214 3 1 1 }'));
ENDSEC;

DATA;
#10=MECHANICAL_DESIGN_GEOMETRIC_PRESENTATION_REPRESENTATION('',(#281),#4777);
#247=SHAPE_REPRESENTATION_RELATIONSHIP('SRR','None',#4876,#264);
#264=ADVANCED_BREP_SHAPE_REPRESENTATION('',(#305),#4761);
#281=STYLED_ITEM('',(#5063),#305);
#305=MANIFOLD_SOLID_BREP('Body1',#2368);
#338=FACE_BOUND('',#637,.T.);
#339=FACE_BOUND('',#639,.T.);
#386=PLANE('',#2642);
#387=PLANE('',#2643);
#473=FACE_OUTER_BOUND('',#634,.T.);
#474=FACE_OUTER_BOUND('',#635,.T.);
#475=FACE_OUTER_BOUND('',#636,.T.);
#476=FACE_OUTER_BOUND('',#638,.T.);
#634=EDGE_LOOP('',(#1751,#1752,#1753,#1754));
#635=EDGE_LOOP('',(#1755,#1756,#1757,#1758));
#636=EDGE_LOOP('',(#1759));
#637=EDGE_LOOP('',(#1760));
#638=EDGE_LOOP('',(#1761));
#639=EDGE_LOOP('',(#1762));
#820=LINE('',#3907,#943);
#821=LINE('',#3913,#944);
#943=VECTOR('',#3093,0.42);
#944=VECTOR('',#3100,0.8);
#1043=CIRCLE('',#2637,0.42);
#1044=CIRCLE('',#2638,0.42);
#1045=CIRCLE('',#2640,0.8);
#1046=CIRCLE('',#2641,0.8);
#1203=VERTEX_POINT('',#3904);
#1204=VERTEX_POINT('',#3906);
#1205=VERTEX_POINT('',#3910);
#1206=VERTEX_POINT('',#3912);
#1413=EDGE_CURVE('',#1203,#1203,#1043,.T.);
#1414=EDGE_CURVE('',#1203,#1204,#820,.T.);
#1415=EDGE_CURVE('',#1204,#1204,#1044,.T.);
#1416=EDGE_CURVE('',#1205,#1205,#1045,.T.);
#1417=EDGE_CURVE('',#1205,#1206,#821,.T.);
#1418=EDGE_CURVE('',#1206,#1206,#1046,.T.);
#1751=ORIENTED_EDGE('',*,*,#1413,.F.);
#1752=ORIENTED_EDGE('',*,*,#1414,.T.);
#1753=ORIENTED_EDGE('',*,*,#1415,.T.);
#1754=ORIENTED_EDGE('',*,*,#1414,.F.);
#1755=ORIENTED_EDGE('',*,*,#1416,.F.);
#1756=ORIENTED_EDGE('',*,*,#1417,.T.);
#1757=ORIENTED_EDGE('',*,*,#1418,.T.);
#1758=ORIENTED_EDGE('',*,*,#1417,.F.);
#1759=ORIENTED_EDGE('',*,*,#1416,.T.);
#1760=ORIENTED_EDGE('',*,*,#1413,.T.);
#1761=ORIENTED_EDGE('',*,*,#1418,.F.);
#1762=ORIENTED_EDGE('',*,*,#1415,.F.);
#2185=CYLINDRICAL_SURFACE('',#2636,0.42);
#2186=CYLINDRICAL_SURFACE('',#2639,0.8);
#2249=ADVANCED_FACE('',(#473),#2185,.F.);
#2250=ADVANCED_FACE('',(#474),#2186,.T.);
#2251=ADVANCED_FACE('',(#475,#338),#386,.T.);
#2252=ADVANCED_FACE('',(#476,#339),#387,.F.);
#2368=CLOSED_SHELL('',(#2249,#2250,#2251,#2252));
#2635=AXIS2_PLACEMENT_3D('',#3902,#3087,#3088);
#2636=AXIS2_PLACEMENT_3D('',#3903,#3089,#3090);
#2637=AXIS2_PLACEMENT_3D('',#3905,#3091,#3092);
#2638=AXIS2_PLACEMENT_3D('',#3908,#3094,#3095);
#2639=AXIS2_PLACEMENT_3D('',#3909,#3096,#3097);
#2640=AXIS2_PLACEMENT_3D('',#3911,#3098,#3099);
#2641=AXIS2_PLACEMENT_3D('',#3914,#3101,#3102);
#2642=AXIS2_PLACEMENT_3D('',#3915,#3103,#3104);
#2643=AXIS2_PLACEMENT_3D('',#3916,#3105,#3106);
#3087=DIRECTION('axis',(0.,0.,1.));
#3088=DIRECTION('refdir',(1.,0.,0.));
#3089=DIRECTION('center_axis',(0.,1.,0.));
#3090=DIRECTION('ref_axis',(1.,0.,0.));
#3091=DIRECTION('center_axis',(0.,-1.,0.));
#3092=DIRECTION('ref_axis',(1.,0.,0.));
#3093=DIRECTION('',(0.,-1.,0.));
#3094=DIRECTION('center_axis',(0.,-1.,0.));
#3095=DIRECTION('ref_axis',(1.,0.,0.));
#3096=DIRECTION('center_axis',(0.,1.,0.));
#3097=DIRECTION('ref_axis',(1.,0.,0.));
#3098=DIRECTION('center_axis',(0.,1.,0.));
#3099=DIRECTION('ref_axis',(1.,0.,0.));
#3100=DIRECTION('',(0.,-1.,0.));
#3101=DIRECTION('center_axis',(0.,1.,0.));
#3102=DIRECTION('ref_axis',(1.,0.,0.));
#3103=DIRECTION('center_axis',(0.,1.,0.));
#3104=DIRECTION('ref_axis',(1.,0.,0.));
#3105=DIRECTION('center_axis',(0.,1.,0.));
#3106=DIRECTION('ref_axis',(1.,0.,0.));
#3902=CARTESIAN_POINT('',(0.,0.,0.));
#3903=CARTESIAN_POINT('Origin',(0.,0.,0.));
#3904=CARTESIAN_POINT('',(-0.42,0.16,5.14351655641888E-17));
#3905=CARTESIAN_POINT('Origin',(0.,0.16,0.));
#3906=CARTESIAN_POINT('',(-0.42,0.,5.14351655641888E-17));
#3907=CARTESIAN_POINT('',(-0.42,0.,5.14351655641888E-17));
#3908=CARTESIAN_POINT('Origin',(0.,0.,0.));
#3909=CARTESIAN_POINT('Origin',(0.,0.,0.));
#3910=CARTESIAN_POINT('',(-0.8,0.16,9.79717439317883E-17));
#3911=CARTESIAN_POINT('Origin',(0.,0.16,0.));
#3912=CARTESIAN_POINT('',(-0.8,0.,9.79717439317883E-17));
#3913=CARTESIAN_POINT('',(-0.8,0.,9.79717439317883E-17));
#3914=CARTESIAN_POINT('Origin',(0.,0.,0.));
#3915=CARTESIAN_POINT('Origin',(0.,0.16,0.));
#3916=CARTESIAN_POINT('Origin',(0.,0.,0.));
#4739=UNCERTAINTY_MEASURE_WITH_UNIT(LENGTH_MEASURE(0.001),#4778,
'DISTANCE_ACCURACY_VALUE',
'Maximum model space distance between geometric entities at asserted c
onnectivities');
#4755=UNCERTAINTY_MEASURE_WITH_UNIT(LENGTH_MEASURE(0.001),#4778,
'DISTANCE_ACCURACY_VALUE',
'Maximum model space distance between geometric entities at asserted c
onnectivities');
#4761=(
GEOMETRIC_REPRESENTATION_CONTEXT(3)
GLOBAL_UNCERTAINTY_ASSIGNED_CONTEXT((#4739))
GLOBAL_UNIT_ASSIGNED_CONTEXT((#4778,#4780,#4781))
REPRESENTATION_CONTEXT('','3D')
);
#4777=(
GEOMETRIC_REPRESENTATION_CONTEXT(3)
GLOBAL_UNCERTAINTY_ASSIGNED_CONTEXT((#4755))
GLOBAL_UNIT_ASSIGNED_CONTEXT((#4778,#4780,#4781))
REPRESENTATION_CONTEXT('','3D')
);
#4778=(
LENGTH_UNIT()
NAMED_UNIT(*)
SI_UNIT(.CENTI.,.METRE.)
);
#4780=(
NAMED_UNIT(*)
PLANE_ANGLE_UNIT()
SI_UNIT($,.RADIAN.)
);
#4781=(
NAMED_UNIT(*)
SI_UNIT($,.STERADIAN.)
SOLID_ANGLE_UNIT()
);
#4787=SHAPE_DEFINITION_REPRESENTATION(#4808,#4876);
#4808=PRODUCT_DEFINITION_SHAPE('',$,#4898);
#4876=SHAPE_REPRESENTATION('',(#2635),#4761);
#4892=PRODUCT_DEFINITION_CONTEXT('part definition',#4957,'design');
#4898=PRODUCT_DEFINITION('Flat Washer - M8','Flat Washer - M8',#4919,#4892);
#4919=PRODUCT_DEFINITION_FORMATION('',$,#4964);
#4957=APPLICATION_CONTEXT(
'Core Data for Automotive Mechanical Design Process');
#4958=PRODUCT_CONTEXT('part definition',#4957,'mechanical');
#4964=PRODUCT('Flat Washer - M8','Flat Washer - M8','Flat Washer - M8',
(#4958));
#5057=COLOUR_RGB('Black',0.12,0.14,0.17);
#5058=FILL_AREA_STYLE_COLOUR('',#5057);
#5059=FILL_AREA_STYLE('',(#5058));
#5060=SURFACE_STYLE_FILL_AREA(#5059);
#5061=SURFACE_SIDE_STYLE('',(#5060));
#5062=SURFACE_STYLE_USAGE(.BOTH.,#5061);
#5063=PRESENTATION_STYLE_ASSIGNMENT((#5062));
ENDSEC;
END-ISO-10303-21;
